ISO-10303-21;
HEADER;
/* Generated by software containing ST-Developer
 * from STEP Tools, Inc. (www.steptools.com) 
 */

FILE_DESCRIPTION(
/* description */ (''),
/* implementation_level */ '2;1');

FILE_NAME(
/* name */ 'Disc_02.step',
/* time_stamp */ '2026-10-04T16:36:43-07:00',
/* author */ (''),
/* organization */ (''),
/* preprocessor_version */ 'ST-DEVELOPER v20.2',
/* originating_system */ 'Autodesk Translation Framework v15.15.0.0',
/* authorisation */ '');

FILE_SCHEMA (('AUTOMOTIVE_DESIGN { 1 0 10303 214 3 1 1 }'));
ENDSEC;

DATA;
#10=MECHANICAL_DESIGN_GEOMETRIC_PRESENTATION_REPRESENTATION('',(#69),#33474);
#32=(
BOUNDED_CURVE()
B_SPLINE_CURVE(5,(#32307,#32308,#32309,#32310,#32311,#32312,#32313,#32314,
#32315,#32316,#32317,#32318,#32319,#32320,#32321,#32322,#32323,#32324,#32325,
#32326,#32327,#32328,#32329,#32330,#32331),.UNSPECIFIED.,.F.,.F.)
B_SPLINE_CURVE_WITH_KNOTS((6,5,1,1,1,1,1,1,1,1,1,1,1,1,1,1,6),(-0.120132019601874,
0.,0.0666666666666667,0.133333333333333,0.2,0.266666666666667,0.333333333333333,
0.4,0.466666666666667,0.533333333333333,0.6,0.666666666666667,0.733333333333333,
0.8,0.866666666666667,0.933333333333333,1.),.UNSPECIFIED.)
CURVE()
GEOMETRIC_REPRESENTATION_ITEM()
RATIONAL_B_SPLINE_CURVE((1.,1.,1.,1.,1.,1.,1.,1.,1.,1.,1.,1.,1.,1.,1.,1.,
1.,1.,1.,1.,1.,1.,1.,1.,1.))
REPRESENTATION_ITEM('')
);
#49=(
BOUNDED_SURFACE()
B_SPLINE_SURFACE(5,2,((#32081,#32082,#32083,#32084,#32085,#32086,#32087,
#32088,#32089),(#32090,#32091,#32092,#32093,#32094,#32095,#32096,#32097,
#32098),(#32099,#32100,#32101,#32102,#32103,#32104,#32105,#32106,#32107),
(#32108,#32109,#32110,#32111,#32112,#32113,#32114,#32115,#32116),(#32117,
#32118,#32119,#32120,#32121,#32122,#32123,#32124,#32125),(#32126,#32127,
#32128,#32129,#32130,#32131,#32132,#32133,#32134),(#32135,#32136,#32137,
#32138,#32139,#32140,#32141,#32142,#32143),(#32144,#32145,#32146,#32147,
#32148,#32149,#32150,#32151,#32152),(#32153,#32154,#32155,#32156,#32157,
#32158,#32159,#32160,#32161),(#32162,#32163,#32164,#32165,#32166,#32167,
#32168,#32169,#32170),(#32171,#32172,#32173,#32174,#32175,#32176,#32177,
#32178,#32179),(#32180,#32181,#32182,#32183,#32184,#32185,#32186,#32187,
#32188),(#32189,#32190,#32191,#32192,#32193,#32194,#32195,#32196,#32197),
(#32198,#32199,#32200,#32201,#32202,#32203,#32204,#32205,#32206),(#32207,
#32208,#32209,#32210,#32211,#32212,#32213,#32214,#32215),(#32216,#32217,
#32218,#32219,#32220,#32221,#32222,#32223,#32224),(#32225,#32226,#32227,
#32228,#32229,#32230,#32231,#32232,#32233),(#32234,#32235,#32236,#32237,
#32238,#32239,#32240,#32241,#32242),(#32243,#32244,#32245,#32246,#32247,
#32248,#32249,#32250,#32251),(#32252,#32253,#32254,#32255,#32256,#32257,
#32258,#32259,#32260),(#32261,#32262,#32263,#32264,#32265,#32266,#32267,
#32268,#32269),(#32270,#32271,#32272,#32273,#32274,#32275,#32276,#32277,
#32278),(#32279,#32280,#32281,#32282,#32283,#32284,#32285,#32286,#32287),
(#32288,#32289,#32290,#32291,#32292,#32293,#32294,#32295,#32296),(#32297,
#32298,#32299,#32300,#32301,#32302,#32303,#32304,#32305)),.UNSPECIFIED.,
 .F.,.T.,.F.)
B_SPLINE_SURFACE_WITH_KNOTS((6,5,1,1,1,1,1,1,1,1,1,1,1,1,1,1,6),(3,2,2,
2,3),(-0.300330049004687,0.,0.0666666666666667,0.133333333333333,0.2,0.266666666666667,
0.333333333333333,0.4,0.466666666666667,0.533333333333333,0.6,0.666666666666667,
0.733333333333333,0.8,0.866666666666667,0.933333333333333,1.),(0.,1.5707963267949,
3.14159265358979,4.71238898038469,6.28318530717959),.UNSPECIFIED.)
GEOMETRIC_REPRESENTATION_ITEM()
RATIONAL_B_SPLINE_SURFACE(((1.,0.707106781186548,1.,0.707106781186548,1.,
0.707106781186548,1.,0.707106781186548,1.),(1.,0.707106781186548,1.,0.707106781186548,
1.,0.707106781186548,1.,0.707106781186548,1.),(1.,0.707106781186548,1.,
0.707106781186548,1.,0.707106781186548,1.,0.707106781186548,1.),(1.,0.707106781186548,
1.,0.707106781186548,1.,0.707106781186548,1.,0.707106781186548,1.),(1.,
0.707106781186548,1.,0.707106781186548,1.,0.707106781186548,1.,0.707106781186548,
1.),(1.,0.707106781186548,1.,0.707106781186548,1.,0.707106781186548,1.,
0.707106781186548,1.),(1.,0.707106781186548,1.,0.707106781186548,1.,0.707106781186548,
1.,0.707106781186548,1.),(1.,0.707106781186548,1.,0.707106781186548,1.,
0.707106781186548,1.,0.707106781186548,1.),(1.,0.707106781186548,1.,0.707106781186548,
1.,0.707106781186548,1.,0.707106781186548,1.),(1.,0.707106781186548,1.,
0.707106781186548,1.,0.707106781186548,1.,0.707106781186548,1.),(1.,0.707106781186548,
1.,0.707106781186548,1.,0.707106781186548,1.,0.707106781186548,1.),(1.,
0.707106781186548,1.,0.707106781186548,1.,0.707106781186548,1.,0.707106781186548,
1.),(1.,0.707106781186548,1.,0.707106781186548,1.,0.707106781186548,1.,
0.707106781186548,1.),(1.,0.707106781186548,1.,0.707106781186548,1.,0.707106781186548,
1.,0.707106781186548,1.),(1.,0.707106781186548,1.,0.707106781186548,1.,
0.707106781186548,1.,0.707106781186548,1.),(1.,0.707106781186548,1.,0.707106781186548,
1.,0.707106781186548,1.,0.707106781186548,1.),(1.,0.707106781186548,1.,
0.707106781186548,1.,0.707106781186548,1.,0.707106781186548,1.),(1.,0.707106781186548,
1.,0.707106781186548,1.,0.707106781186548,1.,0.707106781186548,1.),(1.,
0.707106781186548,1.,0.707106781186548,1.,0.707106781186548,1.,0.707106781186548,
1.),(1.,0.707106781186548,1.,0.707106781186548,1.,0.707106781186548,1.,
0.707106781186548,1.),(1.,0.707106781186548,1.,0.707106781186548,1.,0.707106781186548,
1.,0.707106781186548,1.),(1.,0.707106781186548,1.,0.707106781186548,1.,
0.707106781186548,1.,0.707106781186548,1.),(1.,0.707106781186548,1.,0.707106781186548,
1.,0.707106781186548,1.,0.707106781186548,1.),(1.,0.707106781186548,1.,
0.707106781186548,1.,0.707106781186548,1.,0.707106781186548,1.),(1.,0.707106781186548,
1.,0.707106781186548,1.,0.707106781186548,1.,0.707106781186548,1.)))
REPRESENTATION_ITEM('')
SURFACE()
);
#50=(
BOUNDED_SURFACE()
B_SPLINE_SURFACE(3,2,((#32417,#32418,#32419,#32420,#32421,#32422,#32423,
#32424,#32425),(#32426,#32427,#32428,#32429,#32430,#32431,#32432,#32433,
#32434),(#32435,#32436,#32437,#32438,#32439,#32440,#32441,#32442,#32443),
(#32444,#32445,#32446,#32447,#32448,#32449,#32450,#32451,#32452),(#32453,
#32454,#32455,#32456,#32457,#32458,#32459,#32460,#32461),(#32462,#32463,
#32464,#32465,#32466,#32467,#32468,#32469,#32470),(#32471,#32472,#32473,
#32474,#32475,#32476,#32477,#32478,#32479),(#32480,#32481,#32482,#32483,
#32484,#32485,#32486,#32487,#32488),(#32489,#32490,#32491,#32492,#32493,
#32494,#32495,#32496,#32497),(#32498,#32499,#32500,#32501,#32502,#32503,
#32504,#32505,#32506),(#32507,#32508,#32509,#32510,#32511,#32512,#32513,
#32514,#32515),(#32516,#32517,#32518,#32519,#32520,#32521,#32522,#32523,
#32524),(#32525,#32526,#32527,#32528,#32529,#32530,#32531,#32532,#32533)),
 .UNSPECIFIED.,.F.,.T.,.F.)
B_SPLINE_SURFACE_WITH_KNOTS((4,3,3,3,4),(3,2,2,2,3),(-0.984123122879426,
-0.97309206569331,-0.499330519660681,-0.00706539599512239,0.297293368863902),
(0.,1.5707963267949,3.14159265358979,4.71238898038469,6.28318530717959),
 .UNSPECIFIED.)
GEOMETRIC_REPRESENTATION_ITEM()
RATIONAL_B_SPLINE_SURFACE(((1.,0.707106781186548,1.,0.707106781186548,1.,
0.707106781186548,1.,0.707106781186548,1.),(1.,0.707106781186548,1.,0.707106781186548,
1.,0.707106781186548,1.,0.707106781186548,1.),(1.,0.707106781186548,1.,
0.707106781186548,1.,0.707106781186548,1.,0.707106781186548,1.),(1.,0.707106781186548,
1.,0.707106781186548,1.,0.707106781186548,1.,0.707106781186548,1.),(1.,
0.707106781186548,1.,0.707106781186548,1.,0.707106781186548,1.,0.707106781186548,
1.),(1.,0.707106781186548,1.,0.707106781186548,1.,0.707106781186548,1.,
0.707106781186548,1.),(1.,0.707106781186548,1.,0.707106781186548,1.,0.707106781186548,
1.,0.707106781186548,1.),(1.,0.707106781186548,1.,0.707106781186548,1.,
0.707106781186548,1.,0.707106781186548,1.),(1.,0.707106781186548,1.,0.707106781186548,
1.,0.707106781186548,1.,0.707106781186548,1.),(1.,0.707106781186548,1.,
0.707106781186548,1.,0.707106781186548,1.,0.707106781186548,1.),(1.,0.707106781186548,
1.,0.707106781186548,1.,0.707106781186548,1.,0.707106781186548,1.),(1.,
0.707106781186548,1.,0.707106781186548,1.,0.707106781186548,1.,0.707106781186548,
1.),(1.,0.707106781186548,1.,0.707106781186548,1.,0.707106781186548,1.,
0.707106781186548,1.)))
REPRESENTATION_ITEM('')
SURFACE()
);
#53=CONICAL_SURFACE('',#3108,16.067990296595,0.959931088596882);
#54=CONICAL_SURFACE('',#3114,15.7712719335665,0.959931088596882);
#59=SHAPE_REPRESENTATION_RELATIONSHIP('SRR','None',#33499,#64);
#64=ADVANCED_BREP_SHAPE_REPRESENTATION('',(#74),#33471);
#69=STYLED_ITEM('',(#33531),#74);
#74=MANIFOLD_SOLID_BREP('Body1',#2809);
#81=TOROIDAL_SURFACE('',#3111,16.9386060980155,0.25);
#82=TOROIDAL_SURFACE('',#3116,13.4131653526691,1.72390117308562);
#83=TOROIDAL_SURFACE('',#3123,13.4131653526691,2.22390117308562);
#190=LINE('',#32065,#287);
#191=LINE('',#32074,#288);
#192=LINE('',#32416,#289);
#287=VECTOR('',#3718,16.067990296595);
#288=VECTOR('',#3731,15.7712719335665);
#289=VECTOR('',#3742,3.5);
#398=FACE_OUTER_BOUND('',#521,.T.);
#399=FACE_OUTER_BOUND('',#522,.T.);
#400=FACE_OUTER_BOUND('',#523,.T.);
#401=FACE_OUTER_BOUND('',#524,.T.);
#402=FACE_OUTER_BOUND('',#525,.T.);
#403=FACE_OUTER_BOUND('',#526,.T.);
#404=FACE_OUTER_BOUND('',#527,.T.);
#405=FACE_OUTER_BOUND('',#528,.T.);
#521=EDGE_LOOP('',(#2499,#2500,#2501,#2502));
#522=EDGE_LOOP('',(#2503,#2504,#2505,#2506));
#523=EDGE_LOOP('',(#2507,#2508,#2509,#2510));
#524=EDGE_LOOP('',(#2511,#2512,#2513,#2514,#2515));
#525=EDGE_LOOP('',(#2516,#2517,#2518,#2519,#2520,#2521));
#526=EDGE_LOOP('',(#2522,#2523,#2524,#2525,#2526,#2527));
#527=EDGE_LOOP('',(#2528,#2529,#2530,#2531,#2532,#2533));
#528=EDGE_LOOP('',(#2534,#2535,#2536,#2537,#2538));
#686=CIRCLE('',#3109,17.0820002071033);
#687=CIRCLE('',#3110,14.8491923750145);
#688=CIRCLE('',#3112,16.7952119889278);
#689=CIRCLE('',#3113,0.25);
#690=CIRCLE('',#3115,14.542543867133);
#691=CIRCLE('',#3117,12.2837868382051);
#692=CIRCLE('',#3118,12.2837868382051);
#693=CIRCLE('',#3119,1.72390117308562);
#694=CIRCLE('',#3121,12.0671767507335);
#695=CIRCLE('',#3122,12.0671767507335);
#696=CIRCLE('',#3124,2.22390117308562);
#880=B_SPLINE_CURVE_WITH_KNOTS('',3,(#32333,#32334,#32335,#32336,#32337,
#32338,#32339,#32340,#32341,#32342,#32343,#32344,#32345,#32346,#32347,#32348,
#32349,#32350,#32351,#32352),.UNSPECIFIED.,.F.,.F.,(4,2,2,2,2,2,2,2,2,4),
(-0.787824152103525,-0.776665386905323,-0.683544248464441,-0.586951582106689,
-0.487645947294414,-0.388535605921421,-0.295627476504987,-0.199263976847017,
-0.0990296104815162,0.),.UNSPECIFIED.);
#881=B_SPLINE_CURVE_WITH_KNOTS('',3,(#32353,#32354,#32355,#32356,#32357,
#32358,#32359,#32360,#32361,#32362,#32363,#32364,#32365,#32366,#32367,#32368,
#32369,#32370,#32371,#32372),.UNSPECIFIED.,.F.,.F.,(4,2,2,2,2,2,2,2,2,4),
(0.,0.055050040073654,0.113849056000797,0.210816540693217,0.310109597556882,
0.410211670547242,0.503527973053949,0.600331621930533,0.699630608578637,
0.787671103816308),.UNSPECIFIED.);
#882=B_SPLINE_CURVE_WITH_KNOTS('',3,(#32376,#32377,#32378,#32379,#32380,
#32381,#32382,#32383,#32384,#32385,#32386,#32387,#32388,#32389,#32390,#32391,
#32392,#32393,#32394,#32395),.UNSPECIFIED.,.F.,.F.,(4,2,2,2,2,2,2,2,2,4),
(-0.787824152103524,-0.776665386905322,-0.683544248464441,-0.586951582106688,
-0.487645947294414,-0.388535605921421,-0.295627476504987,-0.199263976847017,
-0.0990296104815161,0.),.UNSPECIFIED.);
#883=B_SPLINE_CURVE_WITH_KNOTS('',3,(#32396,#32397,#32398,#32399,#32400,
#32401,#32402,#32403,#32404,#32405,#32406,#32407,#32408,#32409,#32410,#32411,
#32412,#32413,#32414,#32415),.UNSPECIFIED.,.F.,.F.,(4,2,2,2,2,2,2,2,2,4),
(0.,0.0550500400736524,0.113849056000793,0.210816540693213,0.310109597556877,
0.410211670547238,0.503527973053945,0.600331621930529,0.699630608578633,
0.787671103816303),.UNSPECIFIED.);
#884=B_SPLINE_CURVE_WITH_KNOTS('',3,(#32535,#32536,#32537,#32538,#32539,
#32540,#32541,#32542,#32543,#32544,#32545,#32546,#32547),.UNSPECIFIED.,
 .F.,.F.,(4,3,3,3,4),(-0.114678109950223,0.00706539599431312,0.499330519660279,
0.973092065693301,0.984123122879426),.UNSPECIFIED.);
#1199=VERTEX_POINT('',#32062);
#1200=VERTEX_POINT('',#32064);
#1201=VERTEX_POINT('',#32068);
#1202=VERTEX_POINT('',#32072);
#1203=VERTEX_POINT('',#32076);
#1204=VERTEX_POINT('',#32077);
#1205=VERTEX_POINT('',#32306);
#1206=VERTEX_POINT('',#32332);
#1207=VERTEX_POINT('',#32374);
#1208=VERTEX_POINT('',#32375);
#1209=VERTEX_POINT('',#32534);
#1210=VERTEX_POINT('',#32548);
#1637=EDGE_CURVE('',#1199,#1199,#686,.T.);
#1638=EDGE_CURVE('',#1199,#1200,#190,.T.);
#1639=EDGE_CURVE('',#1200,#1200,#687,.T.);
#1640=EDGE_CURVE('',#1201,#1201,#688,.T.);
#1641=EDGE_CURVE('',#1201,#1199,#689,.T.);
#1642=EDGE_CURVE('',#1202,#1202,#690,.T.);
#1643=EDGE_CURVE('',#1202,#1201,#191,.T.);
#1644=EDGE_CURVE('',#1203,#1204,#691,.T.);
#1645=EDGE_CURVE('',#1204,#1203,#692,.T.);
#1646=EDGE_CURVE('',#1204,#1202,#693,.T.);
#1647=EDGE_CURVE('',#1205,#1203,#32,.T.);
#1648=EDGE_CURVE('',#1206,#1205,#880,.F.);
#1649=EDGE_CURVE('',#1205,#1206,#881,.F.);
#1650=EDGE_CURVE('',#1207,#1208,#882,.T.);
#1651=EDGE_CURVE('',#1208,#1207,#883,.T.);
#1652=EDGE_CURVE('',#1208,#1206,#192,.T.);
#1653=EDGE_CURVE('',#1207,#1209,#884,.T.);
#1654=EDGE_CURVE('',#1210,#1209,#694,.T.);
#1655=EDGE_CURVE('',#1209,#1210,#695,.T.);
#1656=EDGE_CURVE('',#1200,#1210,#696,.T.);
#2499=ORIENTED_EDGE('',*,*,#1637,.F.);
#2500=ORIENTED_EDGE('',*,*,#1638,.T.);
#2501=ORIENTED_EDGE('',*,*,#1639,.T.);
#2502=ORIENTED_EDGE('',*,*,#1638,.F.);
#2503=ORIENTED_EDGE('',*,*,#1640,.T.);
#2504=ORIENTED_EDGE('',*,*,#1641,.T.);
#2505=ORIENTED_EDGE('',*,*,#1637,.T.);
#2506=ORIENTED_EDGE('',*,*,#1641,.F.);
#2507=ORIENTED_EDGE('',*,*,#1642,.F.);
#2508=ORIENTED_EDGE('',*,*,#1643,.T.);
#2509=ORIENTED_EDGE('',*,*,#1640,.F.);
#2510=ORIENTED_EDGE('',*,*,#1643,.F.);
#2511=ORIENTED_EDGE('',*,*,#1644,.F.);
#2512=ORIENTED_EDGE('',*,*,#1645,.F.);
#2513=ORIENTED_EDGE('',*,*,#1646,.T.);
#2514=ORIENTED_EDGE('',*,*,#1642,.T.);
#2515=ORIENTED_EDGE('',*,*,#1646,.F.);
#2516=ORIENTED_EDGE('',*,*,#1647,.T.);
#2517=ORIENTED_EDGE('',*,*,#1644,.T.);
#2518=ORIENTED_EDGE('',*,*,#1645,.T.);
#2519=ORIENTED_EDGE('',*,*,#1647,.F.);
#2520=ORIENTED_EDGE('',*,*,#1648,.F.);
#2521=ORIENTED_EDGE('',*,*,#1649,.F.);
#2522=ORIENTED_EDGE('',*,*,#1650,.F.);
#2523=ORIENTED_EDGE('',*,*,#1651,.F.);
#2524=ORIENTED_EDGE('',*,*,#1652,.T.);
#2525=ORIENTED_EDGE('',*,*,#1648,.T.);
#2526=ORIENTED_EDGE('',*,*,#1649,.T.);
#2527=ORIENTED_EDGE('',*,*,#1652,.F.);
#2528=ORIENTED_EDGE('',*,*,#1653,.F.);
#2529=ORIENTED_EDGE('',*,*,#1650,.T.);
#2530=ORIENTED_EDGE('',*,*,#1651,.T.);
#2531=ORIENTED_EDGE('',*,*,#1653,.T.);
#2532=ORIENTED_EDGE('',*,*,#1654,.F.);
#2533=ORIENTED_EDGE('',*,*,#1655,.F.);
#2534=ORIENTED_EDGE('',*,*,#1639,.F.);
#2535=ORIENTED_EDGE('',*,*,#1656,.T.);
#2536=ORIENTED_EDGE('',*,*,#1654,.T.);
#2537=ORIENTED_EDGE('',*,*,#1655,.T.);
#2538=ORIENTED_EDGE('',*,*,#1656,.F.);
#2684=CYLINDRICAL_SURFACE('',#3120,2.5);
#2785=ADVANCED_FACE('',(#398),#53,.T.);
#2786=ADVANCED_FACE('',(#399),#81,.T.);
#2787=ADVANCED_FACE('',(#400),#54,.F.);
#2788=ADVANCED_FACE('',(#401),#82,.F.);
#2789=ADVANCED_FACE('',(#402),#49,.T.);
#2790=ADVANCED_FACE('',(#403),#2684,.F.);
#2791=ADVANCED_FACE('',(#404),#50,.T.);
#2792=ADVANCED_FACE('',(#405),#83,.T.);
#2809=CLOSED_SHELL('',(#2785,#2786,#2787,#2788,#2789,#2790,#2791,#2792));
#3107=AXIS2_PLACEMENT_3D('',#32060,#3712,#3713);
#3108=AXIS2_PLACEMENT_3D('',#32061,#3714,#3715);
#3109=AXIS2_PLACEMENT_3D('',#32063,#3716,#3717);
#3110=AXIS2_PLACEMENT_3D('',#32066,#3719,#3720);
#3111=AXIS2_PLACEMENT_3D('',#32067,#3721,#3722);
#3112=AXIS2_PLACEMENT_3D('',#32069,#3723,#3724);
#3113=AXIS2_PLACEMENT_3D('',#32070,#3725,#3726);
#3114=AXIS2_PLACEMENT_3D('',#32071,#3727,#3728);
#3115=AXIS2_PLACEMENT_3D('',#32073,#3729,#3730);
#3116=AXIS2_PLACEMENT_3D('',#32075,#3732,#3733);
#3117=AXIS2_PLACEMENT_3D('',#32078,#3734,#3735);
#3118=AXIS2_PLACEMENT_3D('',#32079,#3736,#3737);
#3119=AXIS2_PLACEMENT_3D('',#32080,#3738,#3739);
#3120=AXIS2_PLACEMENT_3D('',#32373,#3740,#3741);
#3121=AXIS2_PLACEMENT_3D('',#32549,#3743,#3744);
#3122=AXIS2_PLACEMENT_3D('',#32550,#3745,#3746);
#3123=AXIS2_PLACEMENT_3D('',#32551,#3747,#3748);
#3124=AXIS2_PLACEMENT_3D('',#32552,#3749,#3750);
#3712=DIRECTION('axis',(0.,0.,1.));
#3713=DIRECTION('refdir',(1.,0.,0.));
#3714=DIRECTION('center_axis',(1.22464679914735E-16,0.,-1.));
#3715=DIRECTION('ref_axis',(-1.,0.,-1.22464679914735E-16));
#3716=DIRECTION('center_axis',(1.22464679914735E-16,0.,-1.));
#3717=DIRECTION('ref_axis',(1.,0.,1.22464679914735E-16));
#3718=DIRECTION('',(-0.819152044288992,1.00317192905353E-16,0.573576436351045));
#3719=DIRECTION('center_axis',(1.22464679914735E-16,0.,-1.));
#3720=DIRECTION('ref_axis',(-1.,0.,-1.22464679914735E-16));
#3721=DIRECTION('center_axis',(1.22464679914735E-16,0.,-1.));
#3722=DIRECTION('ref_axis',(-1.,0.,-2.06690039817172E-16));
#3723=DIRECTION('center_axis',(-1.22464679914735E-16,0.,1.));
#3724=DIRECTION('ref_axis',(1.,0.,1.22464679914735E-16));
#3725=DIRECTION('center_axis',(-1.22464679914735E-16,-1.,-1.49975978266185E-32));
#3726=DIRECTION('ref_axis',(1.,-1.22464679914735E-16,0.));
#3727=DIRECTION('center_axis',(1.22464679914735E-16,0.,-1.));
#3728=DIRECTION('ref_axis',(-1.,0.,-1.22464679914735E-16));
#3729=DIRECTION('center_axis',(1.22464679914735E-16,0.,-1.));
#3730=DIRECTION('ref_axis',(-1.,0.,-1.22464679914735E-16));
#3731=DIRECTION('',(0.819152044288992,-1.00317192905353E-16,-0.573576436351045));
#3732=DIRECTION('center_axis',(1.22464679914735E-16,0.,-1.));
#3733=DIRECTION('ref_axis',(-1.,0.,0.));
#3734=DIRECTION('center_axis',(1.22464679914735E-16,0.,-1.));
#3735=DIRECTION('ref_axis',(-1.,0.,-1.22464679914735E-16));
#3736=DIRECTION('center_axis',(1.22464679914735E-16,0.,-1.));
#3737=DIRECTION('ref_axis',(-1.,0.,-1.22464679914735E-16));
#3738=DIRECTION('center_axis',(1.22464679914735E-16,1.,1.49975978266185E-32));
#3739=DIRECTION('ref_axis',(1.,-1.22464679914735E-16,0.));
#3740=DIRECTION('center_axis',(1.22464679914735E-16,0.,-1.));
#3741=DIRECTION('ref_axis',(-1.,0.,-1.22464679914735E-16));
#3742=DIRECTION('',(1.22464679914735E-16,0.,-1.));
#3743=DIRECTION('center_axis',(1.22464679914735E-16,0.,-1.));
#3744=DIRECTION('ref_axis',(-1.,0.,-1.22464679914735E-16));
#3745=DIRECTION('center_axis',(1.22464679914735E-16,0.,-1.));
#3746=DIRECTION('ref_axis',(-1.,0.,-1.22464679914735E-16));
#3747=DIRECTION('center_axis',(1.22464679914735E-16,0.,-1.));
#3748=DIRECTION('ref_axis',(-1.,0.,0.));
#3749=DIRECTION('center_axis',(-1.22464679914735E-16,-1.,-1.49975978266185E-32));
#3750=DIRECTION('ref_axis',(1.,-1.22464679914735E-16,0.));
#32060=CARTESIAN_POINT('',(0.,0.,0.));
#32061=CARTESIAN_POINT('Origin',(-2.74091738510701E-15,0.,22.3812889317585));
#32062=CARTESIAN_POINT('',(17.0820002071033,-2.09194168766635E-15,21.6712715486013));
#32063=CARTESIAN_POINT('Origin',(-2.65396533354477E-15,-2.09194168766635E-15,
21.6712715486013));
#32064=CARTESIAN_POINT('',(14.8491923750145,-1.81850159119848E-15,23.2347004240035));
#32065=CARTESIAN_POINT('',(16.067990296595,-1.96776128854558E-15,22.3812889317585));
#32066=CARTESIAN_POINT('Origin',(-2.84543015034035E-15,0.,23.2347004240035));
#32067=CARTESIAN_POINT('Origin',(-2.62888603531843E-15,0.,21.466483537529));
#32068=CARTESIAN_POINT('',(16.7952119889278,-2.05682026032416E-15,21.2616955264568));
#32069=CARTESIAN_POINT('Origin',(-2.60380673709209E-15,-2.05682026032416E-15,
21.2616955264568));
#32070=CARTESIAN_POINT('Origin',(16.9386060980155,-2.07438097399525E-15,
21.466483537529));
#32071=CARTESIAN_POINT('Origin',(-2.69161030544755E-15,0.,21.9786660718956));
#32072=CARTESIAN_POINT('',(14.542543867133,-1.78094797983444E-15,22.8390307264222));
#32073=CARTESIAN_POINT('Origin',(-2.79697458747409E-15,0.,22.8390307264222));
#32074=CARTESIAN_POINT('',(15.7712719335665,-1.93142376919247E-15,21.9786660718956));
#32075=CARTESIAN_POINT('Origin',(-2.6374721847239E-15,0.,21.5365947680606));
#32076=CARTESIAN_POINT('',(-12.2837868382052,0.,22.8390307264222));
#32077=CARTESIAN_POINT('',(12.2837868382051,-1.50433002328163E-15,22.8390307264222));
#32078=CARTESIAN_POINT('Origin',(-2.79697458747409E-15,0.,22.8390307264222));
#32079=CARTESIAN_POINT('Origin',(-2.79697458747409E-15,0.,22.8390307264222));
#32080=CARTESIAN_POINT('Origin',(13.4131653526691,-1.64263900155804E-15,
21.5365947680606));
#32081=CARTESIAN_POINT('Ctrl Pts',(-0.999999999999995,0.,20.8266817140213));
#32082=CARTESIAN_POINT('Ctrl Pts',(-0.999999999999995,0.999999999999995,
20.8266817140213));
#32083=CARTESIAN_POINT('Ctrl Pts',(-2.55053290979387E-15,0.999999999999995,
20.8266817140213));
#32084=CARTESIAN_POINT('Ctrl Pts',(0.999999999999995,0.999999999999995,
20.8266817140213));
#32085=CARTESIAN_POINT('Ctrl Pts',(0.999999999999995,0.,20.8266817140213));
#32086=CARTESIAN_POINT('Ctrl Pts',(0.999999999999995,-0.999999999999995,
20.8266817140213));
#32087=CARTESIAN_POINT('Ctrl Pts',(-2.55053290979387E-15,-0.999999999999995,
20.8266817140213));
#32088=CARTESIAN_POINT('Ctrl Pts',(-0.999999999999995,-0.999999999999995,
20.8266817140213));
#32089=CARTESIAN_POINT('Ctrl Pts',(-0.999999999999995,0.,20.8266817140213));
#32090=CARTESIAN_POINT('Ctrl Pts',(-1.5,0.,20.8850056546908));
#32091=CARTESIAN_POINT('Ctrl Pts',(-1.5,1.5,20.8850056546908));
#32092=CARTESIAN_POINT('Ctrl Pts',(-2.5576755325193E-15,1.5,20.8850056546908));
#32093=CARTESIAN_POINT('Ctrl Pts',(1.5,1.5,20.8850056546908));
#32094=CARTESIAN_POINT('Ctrl Pts',(1.5,0.,20.8850056546908));
#32095=CARTESIAN_POINT('Ctrl Pts',(1.5,-1.5,20.8850056546908));
#32096=CARTESIAN_POINT('Ctrl Pts',(-2.5576755325193E-15,-1.5,20.8850056546908));
#32097=CARTESIAN_POINT('Ctrl Pts',(-1.5,-1.5,20.8850056546908));
#32098=CARTESIAN_POINT('Ctrl Pts',(-1.5,0.,20.8850056546908));
#32099=CARTESIAN_POINT('Ctrl Pts',(-2.,0.,20.9433295953604));
#32100=CARTESIAN_POINT('Ctrl Pts',(-2.,2.,20.9433295953604));
#32101=CARTESIAN_POINT('Ctrl Pts',(-2.56481815524472E-15,2.,20.9433295953604));
#32102=CARTESIAN_POINT('Ctrl Pts',(2.,2.,20.9433295953604));
#32103=CARTESIAN_POINT('Ctrl Pts',(2.,0.,20.9433295953604));
#32104=CARTESIAN_POINT('Ctrl Pts',(2.,-2.,20.9433295953604));
#32105=CARTESIAN_POINT('Ctrl Pts',(-2.56481815524472E-15,-2.,20.9433295953604));
#32106=CARTESIAN_POINT('Ctrl Pts',(-2.,-2.,20.9433295953604));
#32107=CARTESIAN_POINT('Ctrl Pts',(-2.,0.,20.9433295953604));
#32108=CARTESIAN_POINT('Ctrl Pts',(-2.5,0.,21.0016535360299));
#32109=CARTESIAN_POINT('Ctrl Pts',(-2.5,2.5,21.0016535360299));
#32110=CARTESIAN_POINT('Ctrl Pts',(-2.57196077797015E-15,2.5,21.0016535360299));
#32111=CARTESIAN_POINT('Ctrl Pts',(2.5,2.5,21.0016535360299));
#32112=CARTESIAN_POINT('Ctrl Pts',(2.5,0.,21.0016535360299));
#32113=CARTESIAN_POINT('Ctrl Pts',(2.5,-2.5,21.0016535360299));
#32114=CARTESIAN_POINT('Ctrl Pts',(-2.57196077797015E-15,-2.5,21.0016535360299));
#32115=CARTESIAN_POINT('Ctrl Pts',(-2.5,-2.5,21.0016535360299));
#32116=CARTESIAN_POINT('Ctrl Pts',(-2.5,0.,21.0016535360299));
#32117=CARTESIAN_POINT('Ctrl Pts',(-3.,0.,21.0599774766995));
#32118=CARTESIAN_POINT('Ctrl Pts',(-3.,3.,21.0599774766995));
#32119=CARTESIAN_POINT('Ctrl Pts',(-2.57910340069557E-15,3.,21.0599774766995));
#32120=CARTESIAN_POINT('Ctrl Pts',(3.,3.,21.0599774766995));
#32121=CARTESIAN_POINT('Ctrl Pts',(3.,0.,21.0599774766995));
#32122=CARTESIAN_POINT('Ctrl Pts',(3.,-3.,21.0599774766995));
#32123=CARTESIAN_POINT('Ctrl Pts',(-2.57910340069557E-15,-3.,21.0599774766995));
#32124=CARTESIAN_POINT('Ctrl Pts',(-3.,-3.,21.0599774766995));
#32125=CARTESIAN_POINT('Ctrl Pts',(-3.,0.,21.0599774766995));
#32126=CARTESIAN_POINT('Ctrl Pts',(-3.5,0.,21.118301417369));
#32127=CARTESIAN_POINT('Ctrl Pts',(-3.5,3.5,21.118301417369));
#32128=CARTESIAN_POINT('Ctrl Pts',(-2.586246023421E-15,3.5,21.118301417369));
#32129=CARTESIAN_POINT('Ctrl Pts',(3.5,3.5,21.118301417369));
#32130=CARTESIAN_POINT('Ctrl Pts',(3.5,0.,21.118301417369));
#32131=CARTESIAN_POINT('Ctrl Pts',(3.5,-3.5,21.118301417369));
#32132=CARTESIAN_POINT('Ctrl Pts',(-2.586246023421E-15,-3.5,21.118301417369));
#32133=CARTESIAN_POINT('Ctrl Pts',(-3.5,-3.5,21.118301417369));
#32134=CARTESIAN_POINT('Ctrl Pts',(-3.5,0.,21.118301417369));
#32135=CARTESIAN_POINT('Ctrl Pts',(-3.61098900507559,0.,21.131248049663));
#32136=CARTESIAN_POINT('Ctrl Pts',(-3.61098900507559,3.61098900507559,21.131248049663));
#32137=CARTESIAN_POINT('Ctrl Pts',(-2.58783152860085E-15,3.61098900507559,
21.131248049663));
#32138=CARTESIAN_POINT('Ctrl Pts',(3.61098900507559,3.61098900507559,21.131248049663));
#32139=CARTESIAN_POINT('Ctrl Pts',(3.61098900507559,0.,21.131248049663));
#32140=CARTESIAN_POINT('Ctrl Pts',(3.61098900507559,-3.61098900507559,21.131248049663));
#32141=CARTESIAN_POINT('Ctrl Pts',(-2.58783152860085E-15,-3.61098900507559,
21.131248049663));
#32142=CARTESIAN_POINT('Ctrl Pts',(-3.61098900507559,-3.61098900507559,
21.131248049663));
#32143=CARTESIAN_POINT('Ctrl Pts',(-3.61098900507559,0.,21.131248049663));
#32144=CARTESIAN_POINT('Ctrl Pts',(-3.83416205501541,0.,21.1582981321148));
#32145=CARTESIAN_POINT('Ctrl Pts',(-3.83416205501541,3.83416205501541,21.1582981321148));
#32146=CARTESIAN_POINT('Ctrl Pts',(-2.59114420828998E-15,3.83416205501541,
21.1582981321148));
#32147=CARTESIAN_POINT('Ctrl Pts',(3.83416205501541,3.83416205501541,21.1582981321148));
#32148=CARTESIAN_POINT('Ctrl Pts',(3.83416205501541,0.,21.1582981321148));
#32149=CARTESIAN_POINT('Ctrl Pts',(3.83416205501541,-3.83416205501541,21.1582981321148));
#32150=CARTESIAN_POINT('Ctrl Pts',(-2.59114420828998E-15,-3.83416205501541,
21.1582981321148));
#32151=CARTESIAN_POINT('Ctrl Pts',(-3.83416205501541,-3.83416205501541,
21.1582981321148));
#32152=CARTESIAN_POINT('Ctrl Pts',(-3.83416205501541,0.,21.1582981321148));
#32153=CARTESIAN_POINT('Ctrl Pts',(-4.17250673641264,0.,21.2023436949734));
#32154=CARTESIAN_POINT('Ctrl Pts',(-4.17250673641264,4.17250673641263,21.2023436949734));
#32155=CARTESIAN_POINT('Ctrl Pts',(-2.59653823404712E-15,4.17250673641263,
21.2023436949734));
#32156=CARTESIAN_POINT('Ctrl Pts',(4.17250673641263,4.17250673641263,21.2023436949734));
#32157=CARTESIAN_POINT('Ctrl Pts',(4.17250673641263,0.,21.2023436949734));
#32158=CARTESIAN_POINT('Ctrl Pts',(4.17250673641263,-4.17250673641263,21.2023436949734));
#32159=CARTESIAN_POINT('Ctrl Pts',(-2.59653823404712E-15,-4.17250673641263,
21.2023436949734));
#32160=CARTESIAN_POINT('Ctrl Pts',(-4.17250673641264,-4.17250673641263,
21.2023436949734));
#32161=CARTESIAN_POINT('Ctrl Pts',(-4.17250673641264,0.,21.2023436949734));
#32162=CARTESIAN_POINT('Ctrl Pts',(-4.63085543889698,0.,21.2680625783243));
#32163=CARTESIAN_POINT('Ctrl Pts',(-4.63085543889698,4.63085543889697,21.2680625783243));
#32164=CARTESIAN_POINT('Ctrl Pts',(-2.60458647606104E-15,4.63085543889697,
21.2680625783243));
#32165=CARTESIAN_POINT('Ctrl Pts',(4.63085543889697,4.63085543889697,21.2680625783243));
#32166=CARTESIAN_POINT('Ctrl Pts',(4.63085543889697,0.,21.2680625783243));
#32167=CARTESIAN_POINT('Ctrl Pts',(4.63085543889697,-4.63085543889697,21.2680625783243));
#32168=CARTESIAN_POINT('Ctrl Pts',(-2.60458647606104E-15,-4.63085543889697,
21.2680625783243));
#32169=CARTESIAN_POINT('Ctrl Pts',(-4.63085543889698,-4.63085543889697,
21.2680625783243));
#32170=CARTESIAN_POINT('Ctrl Pts',(-4.63085543889698,0.,21.2680625783243));
#32171=CARTESIAN_POINT('Ctrl Pts',(-5.21591518523417,0.,21.362025193012));
#32172=CARTESIAN_POINT('Ctrl Pts',(-5.21591518523417,5.21591518523417,21.362025193012));
#32173=CARTESIAN_POINT('Ctrl Pts',(-2.61609357759272E-15,5.21591518523417,
21.362025193012));
#32174=CARTESIAN_POINT('Ctrl Pts',(5.21591518523417,5.21591518523417,21.362025193012));
#32175=CARTESIAN_POINT('Ctrl Pts',(5.21591518523417,0.,21.362025193012));
#32176=CARTESIAN_POINT('Ctrl Pts',(5.21591518523417,-5.21591518523417,21.362025193012));
#32177=CARTESIAN_POINT('Ctrl Pts',(-2.61609357759272E-15,-5.21591518523417,
21.362025193012));
#32178=CARTESIAN_POINT('Ctrl Pts',(-5.21591518523417,-5.21591518523417,
21.362025193012));
#32179=CARTESIAN_POINT('Ctrl Pts',(-5.21591518523417,0.,21.362025193012));
#32180=CARTESIAN_POINT('Ctrl Pts',(-5.81280340273043,0.,21.4677515363784));
#32181=CARTESIAN_POINT('Ctrl Pts',(-5.81280340273043,5.81280340273043,21.4677515363784));
#32182=CARTESIAN_POINT('Ctrl Pts',(-2.62904132039165E-15,5.81280340273043,
21.4677515363784));
#32183=CARTESIAN_POINT('Ctrl Pts',(5.81280340273042,5.81280340273043,21.4677515363784));
#32184=CARTESIAN_POINT('Ctrl Pts',(5.81280340273042,0.,21.4677515363784));
#32185=CARTESIAN_POINT('Ctrl Pts',(5.81280340273042,-5.81280340273043,21.4677515363784));
#32186=CARTESIAN_POINT('Ctrl Pts',(-2.62904132039165E-15,-5.81280340273043,
21.4677515363784));
#32187=CARTESIAN_POINT('Ctrl Pts',(-5.81280340273043,-5.81280340273043,
21.4677515363784));
#32188=CARTESIAN_POINT('Ctrl Pts',(-5.81280340273043,0.,21.4677515363784));
#32189=CARTESIAN_POINT('Ctrl Pts',(-6.42047090449388,0.,21.5847016153273));
#32190=CARTESIAN_POINT('Ctrl Pts',(-6.42047090449388,6.42047090449387,21.5847016153273));
#32191=CARTESIAN_POINT('Ctrl Pts',(-2.64336357437613E-15,6.42047090449388,
21.5847016153273));
#32192=CARTESIAN_POINT('Ctrl Pts',(6.42047090449387,6.42047090449387,21.5847016153273));
#32193=CARTESIAN_POINT('Ctrl Pts',(6.42047090449387,0.,21.5847016153273));
#32194=CARTESIAN_POINT('Ctrl Pts',(6.42047090449387,-6.42047090449387,21.5847016153273));
#32195=CARTESIAN_POINT('Ctrl Pts',(-2.64336357437613E-15,-6.42047090449388,
21.5847016153273));
#32196=CARTESIAN_POINT('Ctrl Pts',(-6.42047090449388,-6.42047090449387,
21.5847016153273));
#32197=CARTESIAN_POINT('Ctrl Pts',(-6.42047090449388,0.,21.5847016153273));
#32198=CARTESIAN_POINT('Ctrl Pts',(-7.0366882084607,0.,21.7115214030506));
#32199=CARTESIAN_POINT('Ctrl Pts',(-7.0366882084607,7.0366882084607,21.7115214030506));
#32200=CARTESIAN_POINT('Ctrl Pts',(-2.65889451908651E-15,7.0366882084607,
21.7115214030506));
#32201=CARTESIAN_POINT('Ctrl Pts',(7.0366882084607,7.0366882084607,21.7115214030506));
#32202=CARTESIAN_POINT('Ctrl Pts',(7.0366882084607,0.,21.7115214030506));
#32203=CARTESIAN_POINT('Ctrl Pts',(7.0366882084607,-7.0366882084607,21.7115214030506));
#32204=CARTESIAN_POINT('Ctrl Pts',(-2.65889451908651E-15,-7.0366882084607,
21.7115214030506));
#32205=CARTESIAN_POINT('Ctrl Pts',(-7.0366882084607,-7.0366882084607,21.7115214030506));
#32206=CARTESIAN_POINT('Ctrl Pts',(-7.0366882084607,0.,21.7115214030506));
#32207=CARTESIAN_POINT('Ctrl Pts',(-7.65759263692165,0.,21.8456924991859));
#32208=CARTESIAN_POINT('Ctrl Pts',(-7.65759263692165,7.65759263692165,21.8456924991859));
#32209=CARTESIAN_POINT('Ctrl Pts',(-2.67532573942854E-15,7.65759263692165,
21.8456924991859));
#32210=CARTESIAN_POINT('Ctrl Pts',(7.65759263692165,7.65759263692165,21.8456924991859));
#32211=CARTESIAN_POINT('Ctrl Pts',(7.65759263692165,0.,21.8456924991859));
#32212=CARTESIAN_POINT('Ctrl Pts',(7.65759263692165,-7.65759263692165,21.8456924991859));
#32213=CARTESIAN_POINT('Ctrl Pts',(-2.67532573942854E-15,-7.65759263692165,
21.8456924991859));
#32214=CARTESIAN_POINT('Ctrl Pts',(-7.65759263692165,-7.65759263692165,
21.8456924991859));
#32215=CARTESIAN_POINT('Ctrl Pts',(-7.65759263692165,0.,21.8456924991859));
#32216=CARTESIAN_POINT('Ctrl Pts',(-8.27837257578008,0.,21.9840162957912));
#32217=CARTESIAN_POINT('Ctrl Pts',(-8.27837257578008,8.27837257578008,21.9840162957912));
#32218=CARTESIAN_POINT('Ctrl Pts',(-2.69226551890439E-15,8.27837257578008,
21.9840162957912));
#32219=CARTESIAN_POINT('Ctrl Pts',(8.27837257578007,8.27837257578008,21.9840162957912));
#32220=CARTESIAN_POINT('Ctrl Pts',(8.27837257578008,0.,21.9840162957912));
#32221=CARTESIAN_POINT('Ctrl Pts',(8.27837257578007,-8.27837257578008,21.9840162957912));
#32222=CARTESIAN_POINT('Ctrl Pts',(-2.69226551890439E-15,-8.27837257578008,
21.9840162957912));
#32223=CARTESIAN_POINT('Ctrl Pts',(-8.27837257578008,-8.27837257578008,
21.9840162957912));
#32224=CARTESIAN_POINT('Ctrl Pts',(-8.27837257578008,0.,21.9840162957912));
#32225=CARTESIAN_POINT('Ctrl Pts',(-8.89388282563607,0.,22.1230393679429));
#32226=CARTESIAN_POINT('Ctrl Pts',(-8.89388282563607,8.89388282563607,22.1230393679429));
#32227=CARTESIAN_POINT('Ctrl Pts',(-2.70929093493621E-15,8.89388282563607,
22.1230393679429));
#32228=CARTESIAN_POINT('Ctrl Pts',(8.89388282563606,8.89388282563607,22.1230393679429));
#32229=CARTESIAN_POINT('Ctrl Pts',(8.89388282563607,0.,22.1230393679429));
#32230=CARTESIAN_POINT('Ctrl Pts',(8.89388282563606,-8.89388282563607,22.1230393679429));
#32231=CARTESIAN_POINT('Ctrl Pts',(-2.70929093493621E-15,-8.89388282563607,
22.1230393679429));
#32232=CARTESIAN_POINT('Ctrl Pts',(-8.89388282563607,-8.89388282563607,
22.1230393679429));
#32233=CARTESIAN_POINT('Ctrl Pts',(-8.89388282563607,0.,22.1230393679429));
#32234=CARTESIAN_POINT('Ctrl Pts',(-9.49928764562852,0.,22.2594854802591));
#32235=CARTESIAN_POINT('Ctrl Pts',(-9.49928764562852,9.49928764562851,22.2594854802591));
#32236=CARTESIAN_POINT('Ctrl Pts',(-2.72600076440663E-15,9.49928764562852,
22.2594854802591));
#32237=CARTESIAN_POINT('Ctrl Pts',(9.49928764562851,9.49928764562851,22.2594854802591));
#32238=CARTESIAN_POINT('Ctrl Pts',(9.49928764562851,0.,22.2594854802591));
#32239=CARTESIAN_POINT('Ctrl Pts',(9.49928764562851,-9.49928764562851,22.2594854802591));
#32240=CARTESIAN_POINT('Ctrl Pts',(-2.72600076440663E-15,-9.49928764562852,
22.2594854802591));
#32241=CARTESIAN_POINT('Ctrl Pts',(-9.49928764562852,-9.49928764562851,
22.2594854802591));
#32242=CARTESIAN_POINT('Ctrl Pts',(-9.49928764562852,0.,22.2594854802591));
#32243=CARTESIAN_POINT('Ctrl Pts',(-10.0906614723548,0.,22.3906513458572));
#32244=CARTESIAN_POINT('Ctrl Pts',(-10.0906614723548,10.0906614723548,22.3906513458572));
#32245=CARTESIAN_POINT('Ctrl Pts',(-2.74206395015284E-15,10.0906614723548,
22.3906513458572));
#32246=CARTESIAN_POINT('Ctrl Pts',(10.0906614723548,10.0906614723548,22.3906513458572));
#32247=CARTESIAN_POINT('Ctrl Pts',(10.0906614723548,0.,22.3906513458572));
#32248=CARTESIAN_POINT('Ctrl Pts',(10.0906614723548,-10.0906614723548,22.3906513458572));
#32249=CARTESIAN_POINT('Ctrl Pts',(-2.74206395015284E-15,-10.0906614723548,
22.3906513458572));
#32250=CARTESIAN_POINT('Ctrl Pts',(-10.0906614723548,-10.0906614723548,
22.3906513458572));
#32251=CARTESIAN_POINT('Ctrl Pts',(-10.0906614723548,0.,22.3906513458572));
#32252=CARTESIAN_POINT('Ctrl Pts',(-10.6657852303826,0.,22.5149133085626));
#32253=CARTESIAN_POINT('Ctrl Pts',(-10.6657852303826,10.6657852303826,22.5149133085626));
#32254=CARTESIAN_POINT('Ctrl Pts',(-2.75728165164113E-15,10.6657852303826,
22.5149133085626));
#32255=CARTESIAN_POINT('Ctrl Pts',(10.6657852303826,10.6657852303826,22.5149133085626));
#32256=CARTESIAN_POINT('Ctrl Pts',(10.6657852303826,0.,22.5149133085626));
#32257=CARTESIAN_POINT('Ctrl Pts',(10.6657852303826,-10.6657852303826,22.5149133085626));
#32258=CARTESIAN_POINT('Ctrl Pts',(-2.75728165164113E-15,-10.6657852303826,
22.5149133085626));
#32259=CARTESIAN_POINT('Ctrl Pts',(-10.6657852303826,-10.6657852303826,
22.5149133085626));
#32260=CARTESIAN_POINT('Ctrl Pts',(-10.6657852303826,0.,22.5149133085626));
#32261=CARTESIAN_POINT('Ctrl Pts',(-11.2237519652345,0.,22.6315014064428));
#32262=CARTESIAN_POINT('Ctrl Pts',(-11.2237519652345,11.2237519652345,22.6315014064428));
#32263=CARTESIAN_POINT('Ctrl Pts',(-2.7715595757299E-15,11.2237519652345,
22.6315014064428));
#32264=CARTESIAN_POINT('Ctrl Pts',(11.2237519652345,11.2237519652345,22.6315014064428));
#32265=CARTESIAN_POINT('Ctrl Pts',(11.2237519652345,0.,22.6315014064428));
#32266=CARTESIAN_POINT('Ctrl Pts',(11.2237519652345,-11.2237519652345,22.6315014064428));
#32267=CARTESIAN_POINT('Ctrl Pts',(-2.7715595757299E-15,-11.2237519652345,
22.6315014064428));
#32268=CARTESIAN_POINT('Ctrl Pts',(-11.2237519652345,-11.2237519652345,
22.6315014064428));
#32269=CARTESIAN_POINT('Ctrl Pts',(-11.2237519652345,0.,22.6315014064428));
#32270=CARTESIAN_POINT('Ctrl Pts',(-11.6562879503402,0.,22.7184407043531));
#32271=CARTESIAN_POINT('Ctrl Pts',(-11.6562879503402,11.6562879503402,22.7184407043531));
#32272=CARTESIAN_POINT('Ctrl Pts',(-2.7822065690205E-15,11.6562879503402,
22.7184407043531));
#32273=CARTESIAN_POINT('Ctrl Pts',(11.6562879503402,11.6562879503402,22.7184407043531));
#32274=CARTESIAN_POINT('Ctrl Pts',(11.6562879503402,0.,22.7184407043531));
#32275=CARTESIAN_POINT('Ctrl Pts',(11.6562879503402,-11.6562879503402,22.7184407043531));
#32276=CARTESIAN_POINT('Ctrl Pts',(-2.7822065690205E-15,-11.6562879503402,
22.7184407043531));
#32277=CARTESIAN_POINT('Ctrl Pts',(-11.6562879503402,-11.6562879503402,
22.7184407043531));
#32278=CARTESIAN_POINT('Ctrl Pts',(-11.6562879503402,0.,22.7184407043531));
#32279=CARTESIAN_POINT('Ctrl Pts',(-11.97300464761,0.,22.7801032581824));
#32280=CARTESIAN_POINT('Ctrl Pts',(-11.97300464761,11.97300464761,22.7801032581824));
#32281=CARTESIAN_POINT('Ctrl Pts',(-2.78975805393792E-15,11.97300464761,
22.7801032581824));
#32282=CARTESIAN_POINT('Ctrl Pts',(11.97300464761,11.97300464761,22.7801032581824));
#32283=CARTESIAN_POINT('Ctrl Pts',(11.97300464761,0.,22.7801032581824));
#32284=CARTESIAN_POINT('Ctrl Pts',(11.97300464761,-11.97300464761,22.7801032581824));
#32285=CARTESIAN_POINT('Ctrl Pts',(-2.78975805393792E-15,-11.97300464761,
22.7801032581824));
#32286=CARTESIAN_POINT('Ctrl Pts',(-11.97300464761,-11.97300464761,22.7801032581824));
#32287=CARTESIAN_POINT('Ctrl Pts',(-11.97300464761,0.,22.7801032581824));
#32288=CARTESIAN_POINT('Ctrl Pts',(-12.1807579618051,0.,22.8196487184886));
#32289=CARTESIAN_POINT('Ctrl Pts',(-12.1807579618051,12.1807579618051,22.8196487184886));
#32290=CARTESIAN_POINT('Ctrl Pts',(-2.79460097607641E-15,12.1807579618051,
22.8196487184886));
#32291=CARTESIAN_POINT('Ctrl Pts',(12.1807579618051,12.1807579618051,22.8196487184886));
#32292=CARTESIAN_POINT('Ctrl Pts',(12.1807579618051,0.,22.8196487184886));
#32293=CARTESIAN_POINT('Ctrl Pts',(12.1807579618051,-12.1807579618051,22.8196487184886));
#32294=CARTESIAN_POINT('Ctrl Pts',(-2.79460097607641E-15,-12.1807579618051,
22.8196487184886));
#32295=CARTESIAN_POINT('Ctrl Pts',(-12.1807579618051,-12.1807579618051,
22.8196487184886));
#32296=CARTESIAN_POINT('Ctrl Pts',(-12.1807579618051,0.,22.8196487184886));
#32297=CARTESIAN_POINT('Ctrl Pts',(-12.2837868382052,0.,22.8390307264222));
#32298=CARTESIAN_POINT('Ctrl Pts',(-12.2837868382052,12.2837868382051,22.8390307264222));
#32299=CARTESIAN_POINT('Ctrl Pts',(-2.79697458747409E-15,12.2837868382051,
22.8390307264222));
#32300=CARTESIAN_POINT('Ctrl Pts',(12.2837868382051,12.2837868382051,22.8390307264222));
#32301=CARTESIAN_POINT('Ctrl Pts',(12.2837868382051,0.,22.8390307264222));
#32302=CARTESIAN_POINT('Ctrl Pts',(12.2837868382051,-12.2837868382051,22.8390307264222));
#32303=CARTESIAN_POINT('Ctrl Pts',(-2.79697458747409E-15,-12.2837868382051,
22.8390307264222));
#32304=CARTESIAN_POINT('Ctrl Pts',(-12.2837868382052,-12.2837868382051,
22.8390307264222));
#32305=CARTESIAN_POINT('Ctrl Pts',(-12.2837868382052,0.,22.8390307264222));
#32306=CARTESIAN_POINT('',(-2.5,0.,21.0016535360299));
#32307=CARTESIAN_POINT('Ctrl Pts',(-2.5,0.,21.0016535360299));
#32308=CARTESIAN_POINT('Ctrl Pts',(-2.7,0.,21.0249831122978));
#32309=CARTESIAN_POINT('Ctrl Pts',(-2.9,0.,21.0483126885656));
#32310=CARTESIAN_POINT('Ctrl Pts',(-3.1,0.,21.0716422648334));
#32311=CARTESIAN_POINT('Ctrl Pts',(-3.3,0.,21.0949718411012));
#32312=CARTESIAN_POINT('Ctrl Pts',(-3.5,0.,21.118301417369));
#32313=CARTESIAN_POINT('Ctrl Pts',(-3.61098900507559,0.,21.131248049663));
#32314=CARTESIAN_POINT('Ctrl Pts',(-3.83416205501541,0.,21.1582981321148));
#32315=CARTESIAN_POINT('Ctrl Pts',(-4.17250673641264,0.,21.2023436949734));
#32316=CARTESIAN_POINT('Ctrl Pts',(-4.63085543889698,0.,21.2680625783243));
#32317=CARTESIAN_POINT('Ctrl Pts',(-5.21591518523417,0.,21.362025193012));
#32318=CARTESIAN_POINT('Ctrl Pts',(-5.81280340273043,0.,21.4677515363784));
#32319=CARTESIAN_POINT('Ctrl Pts',(-6.42047090449388,0.,21.5847016153273));
#32320=CARTESIAN_POINT('Ctrl Pts',(-7.0366882084607,0.,21.7115214030506));
#32321=CARTESIAN_POINT('Ctrl Pts',(-7.65759263692165,0.,21.8456924991859));
#32322=CARTESIAN_POINT('Ctrl Pts',(-8.27837257578008,0.,21.9840162957912));
#32323=CARTESIAN_POINT('Ctrl Pts',(-8.89388282563607,0.,22.1230393679429));
#32324=CARTESIAN_POINT('Ctrl Pts',(-9.49928764562852,0.,22.2594854802591));
#32325=CARTESIAN_POINT('Ctrl Pts',(-10.0906614723548,0.,22.3906513458572));
#32326=CARTESIAN_POINT('Ctrl Pts',(-10.6657852303826,0.,22.5149133085626));
#32327=CARTESIAN_POINT('Ctrl Pts',(-11.2237519652345,0.,22.6315014064428));
#32328=CARTESIAN_POINT('Ctrl Pts',(-11.6562879503402,0.,22.7184407043531));
#32329=CARTESIAN_POINT('Ctrl Pts',(-11.97300464761,0.,22.7801032581824));
#32330=CARTESIAN_POINT('Ctrl Pts',(-12.1807579618051,0.,22.8196487184886));
#32331=CARTESIAN_POINT('Ctrl Pts',(-12.2837868382052,0.,22.8390307264222));
#32332=CARTESIAN_POINT('',(2.5,-3.06161699786838E-16,21.0016535360299));
#32333=CARTESIAN_POINT('Ctrl Pts',(-2.5,-1.47022104461876E-15,21.0016535360299));
#32334=CARTESIAN_POINT('Ctrl Pts',(-2.5,-0.0371231848941886,21.0016535360299));
#32335=CARTESIAN_POINT('Ctrl Pts',(-2.49917312973535,-0.0742778661173672,
21.0016535360299));
#32336=CARTESIAN_POINT('Ctrl Pts',(-2.48367897424576,-0.421532049454882,
21.0016535360299));
#32337=CARTESIAN_POINT('Ctrl Pts',(-2.41221020755755,-0.726355581229533,
21.0016535360299));
#32338=CARTESIAN_POINT('Ctrl Pts',(-2.15665695254898,-1.30479846977776,
21.0016535360299));
#32339=CARTESIAN_POINT('Ctrl Pts',(-1.97086325139701,-1.57142174542834,
21.0016535360299));
#32340=CARTESIAN_POINT('Ctrl Pts',(-1.50189098051651,-2.02580771968822,
21.0016535360299));
#32341=CARTESIAN_POINT('Ctrl Pts',(-1.22075973154356,-2.20665337385529,
21.0016535360299));
#32342=CARTESIAN_POINT('Ctrl Pts',(-0.605012462119601,-2.44808145431904,
21.0016535360299));
#32343=CARTESIAN_POINT('Ctrl Pts',(-0.276566066778985,-2.50652231129252,
21.0016535360299));
#32344=CARTESIAN_POINT('Ctrl Pts',(0.363347686367216,-2.49276727488126,
21.0016535360299));
#32345=CARTESIAN_POINT('Ctrl Pts',(0.669054826467961,-2.42863662722262,
21.0016535360299));
#32346=CARTESIAN_POINT('Ctrl Pts',(1.25208783868412,-2.18756782255767,21.0016535360299));
#32347=CARTESIAN_POINT('Ctrl Pts',(1.52250913573239,-2.00876650352443,21.0016535360299));
#32348=CARTESIAN_POINT('Ctrl Pts',(1.99007168793019,-1.54959582229107,21.0016535360299));
#32349=CARTESIAN_POINT('Ctrl Pts',(2.17912399473894,-1.27005950691937,21.0016535360299));
#32350=CARTESIAN_POINT('Ctrl Pts',(2.43462090831919,-0.656952194285372,
21.0016535360299));
#32351=CARTESIAN_POINT('Ctrl Pts',(2.5,-0.330098701605055,21.0016535360299));
#32352=CARTESIAN_POINT('Ctrl Pts',(2.5,-1.45716771982052E-15,21.0016535360299));
#32353=CARTESIAN_POINT('Ctrl Pts',(2.5,-1.42247325030098E-15,21.0016535360299));
#32354=CARTESIAN_POINT('Ctrl Pts',(2.5,0.183500133578845,21.0016535360299));
#32355=CARTESIAN_POINT('Ctrl Pts',(2.47979662058594,0.36644374677987,21.0016535360299));
#32356=CARTESIAN_POINT('Ctrl Pts',(2.39698708053327,0.736795527885595,21.0016535360299));
#32357=CARTESIAN_POINT('Ctrl Pts',(2.33187346931883,0.922377816972297,21.0016535360299));
#32358=CARTESIAN_POINT('Ctrl Pts',(2.10373946785474,1.38879610419601,21.0016535360299));
#32359=CARTESIAN_POINT('Ctrl Pts',(1.90675062561359,1.6488712561513,21.0016535360299));
#32360=CARTESIAN_POINT('Ctrl Pts',(1.41891687160026,2.08475912057876,21.0016535360299));
#32361=CARTESIAN_POINT('Ctrl Pts',(1.13075556057171,2.25409350772862,21.0016535360299));
#32362=CARTESIAN_POINT('Ctrl Pts',(0.502690476103074,2.47156637397813,21.0016535360299));
#32363=CARTESIAN_POINT('Ctrl Pts',(0.168693444061263,2.51652152338796,21.0016535360299));
#32364=CARTESIAN_POINT('Ctrl Pts',(-0.474641333693119,2.47416054609107,
21.0016535360299));
#32365=CARTESIAN_POINT('Ctrl Pts',(-0.77850055995708,2.395974056961,21.0016535360299));
#32366=CARTESIAN_POINT('Ctrl Pts',(-1.35242509772431,2.12722071777005,21.0016535360299));
#32367=CARTESIAN_POINT('Ctrl Pts',(-1.61541268207329,1.93508746408567,21.0016535360299));
#32368=CARTESIAN_POINT('Ctrl Pts',(-2.05946515295737,1.45539068556724,21.0016535360299));
#32369=CARTESIAN_POINT('Ctrl Pts',(-2.23385447989841,1.17023626952827,21.0016535360299));
#32370=CARTESIAN_POINT('Ctrl Pts',(-2.44852353908426,0.583828854975952,
21.0016535360299));
#32371=CARTESIAN_POINT('Ctrl Pts',(-2.5,0.292894735647856,21.0016535360299));
#32372=CARTESIAN_POINT('Ctrl Pts',(-2.5,-1.52655665885959E-15,21.0016535360299));
#32373=CARTESIAN_POINT('Origin',(-2.61707322499551E-15,0.,21.3700246211203));
#32374=CARTESIAN_POINT('',(-2.49999999999983,4.22182696387148E-32,21.5031612699275));
#32375=CARTESIAN_POINT('',(2.5,-3.06161699786838E-16,21.5031612699274));
#32376=CARTESIAN_POINT('Ctrl Pts',(-2.5,-2.09528118263808E-15,21.5031612699274));
#32377=CARTESIAN_POINT('Ctrl Pts',(-2.5,0.0371231848941853,21.5031612699274));
#32378=CARTESIAN_POINT('Ctrl Pts',(-2.49917312973534,0.0742778661173668,
21.5031612699274));
#32379=CARTESIAN_POINT('Ctrl Pts',(-2.48367897424575,0.421532049454881,
21.5031612699274));
#32380=CARTESIAN_POINT('Ctrl Pts',(-2.41221020755754,0.726355581229531,
21.5031612699274));
#32381=CARTESIAN_POINT('Ctrl Pts',(-2.15665695254898,1.30479846977776,21.5031612699274));
#32382=CARTESIAN_POINT('Ctrl Pts',(-1.97086325139701,1.57142174542834,21.5031612699274));
#32383=CARTESIAN_POINT('Ctrl Pts',(-1.50189098051651,2.02580771968822,21.5031612699274));
#32384=CARTESIAN_POINT('Ctrl Pts',(-1.22075973154356,2.20665337385528,21.5031612699274));
#32385=CARTESIAN_POINT('Ctrl Pts',(-0.605012462119599,2.44808145431903,
21.5031612699274));
#32386=CARTESIAN_POINT('Ctrl Pts',(-0.276566066778986,2.50652231129252,
21.5031612699274));
#32387=CARTESIAN_POINT('Ctrl Pts',(0.363347686367214,2.49276727488126,21.5031612699274));
#32388=CARTESIAN_POINT('Ctrl Pts',(0.669054826467959,2.42863662722262,21.5031612699274));
#32389=CARTESIAN_POINT('Ctrl Pts',(1.25208783868411,2.18756782255767,21.5031612699274));
#32390=CARTESIAN_POINT('Ctrl Pts',(1.52250913573239,2.00876650352443,21.5031612699274));
#32391=CARTESIAN_POINT('Ctrl Pts',(1.99007168793019,1.54959582229107,21.5031612699274));
#32392=CARTESIAN_POINT('Ctrl Pts',(2.17912399473894,1.27005950691937,21.5031612699274));
#32393=CARTESIAN_POINT('Ctrl Pts',(2.43462090831919,0.65695219428537,21.5031612699274));
#32394=CARTESIAN_POINT('Ctrl Pts',(2.5,0.330098701605054,21.5031612699274));
#32395=CARTESIAN_POINT('Ctrl Pts',(2.5,-6.93889390390723E-17,21.5031612699274));
#32396=CARTESIAN_POINT('Ctrl Pts',(2.5,-2.42861286636753E-16,21.5031612699274));
#32397=CARTESIAN_POINT('Ctrl Pts',(2.5,-0.183500133578842,21.5031612699274));
#32398=CARTESIAN_POINT('Ctrl Pts',(2.47979662058591,-0.366443746779858,
21.5031612699274));
#32399=CARTESIAN_POINT('Ctrl Pts',(2.39698708053325,-0.736795527885571,
21.5031612699274));
#32400=CARTESIAN_POINT('Ctrl Pts',(2.33187346931882,-0.922377816972267,
21.5031612699274));
#32401=CARTESIAN_POINT('Ctrl Pts',(2.10373946785474,-1.38879610419597,21.5031612699274));
#32402=CARTESIAN_POINT('Ctrl Pts',(1.90675062561359,-1.64887125615127,21.5031612699274));
#32403=CARTESIAN_POINT('Ctrl Pts',(1.41891687160027,-2.08475912057872,21.5031612699274));
#32404=CARTESIAN_POINT('Ctrl Pts',(1.13075556057173,-2.25409350772859,21.5031612699274));
#32405=CARTESIAN_POINT('Ctrl Pts',(0.502690476103094,-2.4715663739781,21.5031612699274));
#32406=CARTESIAN_POINT('Ctrl Pts',(0.168693444061285,-2.51652152338794,
21.5031612699274));
#32407=CARTESIAN_POINT('Ctrl Pts',(-0.4746413336931,-2.47416054609105,21.5031612699274));
#32408=CARTESIAN_POINT('Ctrl Pts',(-0.778500559957059,-2.39597405696099,
21.5031612699274));
#32409=CARTESIAN_POINT('Ctrl Pts',(-1.35242509772429,-2.12722071777004,
21.5031612699274));
#32410=CARTESIAN_POINT('Ctrl Pts',(-1.61541268207327,-1.93508746408566,
21.5031612699274));
#32411=CARTESIAN_POINT('Ctrl Pts',(-2.05946515295735,-1.45539068556723,
21.5031612699274));
#32412=CARTESIAN_POINT('Ctrl Pts',(-2.23385447989839,-1.17023626952826,
21.5031612699274));
#32413=CARTESIAN_POINT('Ctrl Pts',(-2.44852353908424,-0.583828854975948,
21.5031612699274));
#32414=CARTESIAN_POINT('Ctrl Pts',(-2.5,-0.292894735647858,21.5031612699274));
#32415=CARTESIAN_POINT('Ctrl Pts',(-2.5,-2.28983498828939E-15,21.5031612699274));
#32416=CARTESIAN_POINT('',(2.5,-3.06161699786838E-16,21.3700246211203));
#32417=CARTESIAN_POINT('Ctrl Pts',(-12.0671767507335,0.,23.3069199108271));
#32418=CARTESIAN_POINT('Ctrl Pts',(-12.0671767507335,12.0671767507335,23.3069199108271));
#32419=CARTESIAN_POINT('Ctrl Pts',(-2.85427448667781E-15,12.0671767507335,
23.3069199108271));
#32420=CARTESIAN_POINT('Ctrl Pts',(12.0671767507335,12.0671767507335,23.3069199108271));
#32421=CARTESIAN_POINT('Ctrl Pts',(12.0671767507335,0.,23.3069199108271));
#32422=CARTESIAN_POINT('Ctrl Pts',(12.0671767507335,-12.0671767507335,23.3069199108271));
#32423=CARTESIAN_POINT('Ctrl Pts',(-2.85427448667781E-15,-12.0671767507335,
23.3069199108271));
#32424=CARTESIAN_POINT('Ctrl Pts',(-12.0671767507335,-12.0671767507335,
23.3069199108271));
#32425=CARTESIAN_POINT('Ctrl Pts',(-12.0671767507335,0.,23.3069199108271));
#32426=CARTESIAN_POINT('Ctrl Pts',(-12.0383097771307,0.,23.3014281454301));
#32427=CARTESIAN_POINT('Ctrl Pts',(-12.0383097771307,12.0383097771307,23.3014281454301));
#32428=CARTESIAN_POINT('Ctrl Pts',(-2.85360193938631E-15,12.0383097771307,
23.3014281454301));
#32429=CARTESIAN_POINT('Ctrl Pts',(12.0383097771306,12.0383097771307,23.3014281454301));
#32430=CARTESIAN_POINT('Ctrl Pts',(12.0383097771307,0.,23.3014281454301));
#32431=CARTESIAN_POINT('Ctrl Pts',(12.0383097771306,-12.0383097771307,23.3014281454301));
#32432=CARTESIAN_POINT('Ctrl Pts',(-2.85360193938631E-15,-12.0383097771307,
23.3014281454301));
#32433=CARTESIAN_POINT('Ctrl Pts',(-12.0383097771307,-12.0383097771307,
23.3014281454301));
#32434=CARTESIAN_POINT('Ctrl Pts',(-12.0383097771307,0.,23.3014281454301));
#32435=CARTESIAN_POINT('Ctrl Pts',(-12.0093666549873,0.,23.2959007739165));
#32436=CARTESIAN_POINT('Ctrl Pts',(-12.0093666549873,12.0093666549873,23.2959007739165));
#32437=CARTESIAN_POINT('Ctrl Pts',(-2.85292503160311E-15,12.0093666549873,
23.2959007739165));
#32438=CARTESIAN_POINT('Ctrl Pts',(12.0093666549873,12.0093666549873,23.2959007739165));
#32439=CARTESIAN_POINT('Ctrl Pts',(12.0093666549873,0.,23.2959007739165));
#32440=CARTESIAN_POINT('Ctrl Pts',(12.0093666549873,-12.0093666549873,23.2959007739165));
#32441=CARTESIAN_POINT('Ctrl Pts',(-2.85292503160311E-15,-12.0093666549873,
23.2959007739165));
#32442=CARTESIAN_POINT('Ctrl Pts',(-12.0093666549873,-12.0093666549873,
23.2959007739165));
#32443=CARTESIAN_POINT('Ctrl Pts',(-12.0093666549873,0.,23.2959007739165));
#32444=CARTESIAN_POINT('Ctrl Pts',(-11.9803472472225,0.,23.2903377571183));
#32445=CARTESIAN_POINT('Ctrl Pts',(-11.9803472472225,11.9803472472225,23.2903377571183));
#32446=CARTESIAN_POINT('Ctrl Pts',(-2.85224375853157E-15,11.9803472472225,
23.2903377571183));
#32447=CARTESIAN_POINT('Ctrl Pts',(11.9803472472225,11.9803472472225,23.2903377571183));
#32448=CARTESIAN_POINT('Ctrl Pts',(11.9803472472225,0.,23.2903377571183));
#32449=CARTESIAN_POINT('Ctrl Pts',(11.9803472472225,-11.9803472472225,23.2903377571183));
#32450=CARTESIAN_POINT('Ctrl Pts',(-2.85224375853157E-15,-11.9803472472225,
23.2903377571183));
#32451=CARTESIAN_POINT('Ctrl Pts',(-11.9803472472225,-11.9803472472225,
23.2903377571183));
#32452=CARTESIAN_POINT('Ctrl Pts',(-11.9803472472225,0.,23.2903377571183));
#32453=CARTESIAN_POINT('Ctrl Pts',(-10.7340225064793,0.,23.051417461952));
#32454=CARTESIAN_POINT('Ctrl Pts',(-10.7340225064793,10.7340225064793,23.051417461952));
#32455=CARTESIAN_POINT('Ctrl Pts',(-2.82298446105889E-15,10.7340225064793,
23.051417461952));
#32456=CARTESIAN_POINT('Ctrl Pts',(10.7340225064793,10.7340225064793,23.051417461952));
#32457=CARTESIAN_POINT('Ctrl Pts',(10.7340225064793,0.,23.051417461952));
#32458=CARTESIAN_POINT('Ctrl Pts',(10.7340225064793,-10.7340225064793,23.051417461952));
#32459=CARTESIAN_POINT('Ctrl Pts',(-2.82298446105889E-15,-10.7340225064793,
23.051417461952));
#32460=CARTESIAN_POINT('Ctrl Pts',(-10.7340225064793,-10.7340225064793,
23.051417461952));
#32461=CARTESIAN_POINT('Ctrl Pts',(-10.7340225064793,0.,23.051417461952));
#32462=CARTESIAN_POINT('Ctrl Pts',(-9.31567463360365,0.,22.7265913199738));
#32463=CARTESIAN_POINT('Ctrl Pts',(-9.31567463360365,9.31567463360365,22.7265913199738));
#32464=CARTESIAN_POINT('Ctrl Pts',(-2.78320473155359E-15,9.31567463360365,
22.7265913199738));
#32465=CARTESIAN_POINT('Ctrl Pts',(9.31567463360364,9.31567463360365,22.7265913199738));
#32466=CARTESIAN_POINT('Ctrl Pts',(9.31567463360365,0.,22.7265913199738));
#32467=CARTESIAN_POINT('Ctrl Pts',(9.31567463360364,-9.31567463360365,22.7265913199738));
#32468=CARTESIAN_POINT('Ctrl Pts',(-2.78320473155359E-15,-9.31567463360365,
22.7265913199738));
#32469=CARTESIAN_POINT('Ctrl Pts',(-9.31567463360365,-9.31567463360365,
22.7265913199738));
#32470=CARTESIAN_POINT('Ctrl Pts',(-9.31567463360365,0.,22.7265913199738));
#32471=CARTESIAN_POINT('Ctrl Pts',(-7.85305095226366,0.,22.4018903191022));
#32472=CARTESIAN_POINT('Ctrl Pts',(-7.85305095226366,7.85305095226366,22.4018903191022));
#32473=CARTESIAN_POINT('Ctrl Pts',(-2.74344032741386E-15,7.85305095226366,
22.4018903191022));
#32474=CARTESIAN_POINT('Ctrl Pts',(7.85305095226366,7.85305095226366,22.4018903191022));
#32475=CARTESIAN_POINT('Ctrl Pts',(7.85305095226366,0.,22.4018903191022));
#32476=CARTESIAN_POINT('Ctrl Pts',(7.85305095226366,-7.85305095226366,22.4018903191022));
#32477=CARTESIAN_POINT('Ctrl Pts',(-2.74344032741386E-15,-7.85305095226366,
22.4018903191022));
#32478=CARTESIAN_POINT('Ctrl Pts',(-7.85305095226366,-7.85305095226366,
22.4018903191022));
#32479=CARTESIAN_POINT('Ctrl Pts',(-7.85305095226366,0.,22.4018903191022));
#32480=CARTESIAN_POINT('Ctrl Pts',(-6.33330197010078,0.,22.0645075583296));
#32481=CARTESIAN_POINT('Ctrl Pts',(-6.33330197010078,6.33330197010078,22.0645075583296));
#32482=CARTESIAN_POINT('Ctrl Pts',(-2.70212285560709E-15,6.33330197010078,
22.0645075583296));
#32483=CARTESIAN_POINT('Ctrl Pts',(6.33330197010078,6.33330197010078,22.0645075583296));
#32484=CARTESIAN_POINT('Ctrl Pts',(6.33330197010078,0.,22.0645075583296));
#32485=CARTESIAN_POINT('Ctrl Pts',(6.33330197010078,-6.33330197010078,22.0645075583296));
#32486=CARTESIAN_POINT('Ctrl Pts',(-2.70212285560709E-15,-6.33330197010078,
22.0645075583296));
#32487=CARTESIAN_POINT('Ctrl Pts',(-6.33330197010078,-6.33330197010078,
22.0645075583296));
#32488=CARTESIAN_POINT('Ctrl Pts',(-6.33330197010078,0.,22.0645075583296));
#32489=CARTESIAN_POINT('Ctrl Pts',(-4.84782034806848,0.,21.7815811966328));
#32490=CARTESIAN_POINT('Ctrl Pts',(-4.84782034806848,4.84782034806848,21.7815811966328));
#32491=CARTESIAN_POINT('Ctrl Pts',(-2.66747436928245E-15,4.84782034806848,
21.7815811966328));
#32492=CARTESIAN_POINT('Ctrl Pts',(4.84782034806847,4.84782034806848,21.7815811966328));
#32493=CARTESIAN_POINT('Ctrl Pts',(4.84782034806847,0.,21.7815811966328));
#32494=CARTESIAN_POINT('Ctrl Pts',(4.84782034806847,-4.84782034806848,21.7815811966328));
#32495=CARTESIAN_POINT('Ctrl Pts',(-2.66747436928245E-15,-4.84782034806848,
21.7815811966328));
#32496=CARTESIAN_POINT('Ctrl Pts',(-4.84782034806848,-4.84782034806848,
21.7815811966328));
#32497=CARTESIAN_POINT('Ctrl Pts',(-4.84782034806848,0.,21.7815811966328));
#32498=CARTESIAN_POINT('Ctrl Pts',(-3.50000000000663,0.,21.6217478248724));
#32499=CARTESIAN_POINT('Ctrl Pts',(-3.50000000000662,3.50000000000662,21.6217478248724));
#32500=CARTESIAN_POINT('Ctrl Pts',(-2.64790042657012E-15,3.50000000000662,
21.6217478248724));
#32501=CARTESIAN_POINT('Ctrl Pts',(3.50000000000662,3.50000000000662,21.6217478248724));
#32502=CARTESIAN_POINT('Ctrl Pts',(3.50000000000662,0.,21.6217478248724));
#32503=CARTESIAN_POINT('Ctrl Pts',(3.50000000000662,-3.50000000000662,21.6217478248724));
#32504=CARTESIAN_POINT('Ctrl Pts',(-2.64790042657012E-15,-3.50000000000662,
21.6217478248724));
#32505=CARTESIAN_POINT('Ctrl Pts',(-3.50000000000662,-3.50000000000662,
21.6217478248724));
#32506=CARTESIAN_POINT('Ctrl Pts',(-3.50000000000663,0.,21.6217478248724));
#32507=CARTESIAN_POINT('Ctrl Pts',(-2.6666666666733,0.,21.5229256957522));
#32508=CARTESIAN_POINT('Ctrl Pts',(-2.66666666667328,2.66666666667328,21.5229256957522));
#32509=CARTESIAN_POINT('Ctrl Pts',(-2.63579820615892E-15,2.66666666667328,
21.5229256957522));
#32510=CARTESIAN_POINT('Ctrl Pts',(2.66666666667329,2.66666666667328,21.5229256957522));
#32511=CARTESIAN_POINT('Ctrl Pts',(2.66666666667329,0.,21.5229256957522));
#32512=CARTESIAN_POINT('Ctrl Pts',(2.66666666667329,-2.66666666667328,21.5229256957522));
#32513=CARTESIAN_POINT('Ctrl Pts',(-2.63579820615892E-15,-2.66666666667328,
21.5229256957522));
#32514=CARTESIAN_POINT('Ctrl Pts',(-2.66666666667328,-2.66666666667328,
21.5229256957522));
#32515=CARTESIAN_POINT('Ctrl Pts',(-2.6666666666733,0.,21.5229256957522));
#32516=CARTESIAN_POINT('Ctrl Pts',(-1.83333333333996,0.,21.424103566632));
#32517=CARTESIAN_POINT('Ctrl Pts',(-1.83333333333994,1.83333333333994,21.424103566632));
#32518=CARTESIAN_POINT('Ctrl Pts',(-2.62369598574772E-15,1.83333333333994,
21.424103566632));
#32519=CARTESIAN_POINT('Ctrl Pts',(1.83333333333995,1.83333333333994,21.424103566632));
#32520=CARTESIAN_POINT('Ctrl Pts',(1.83333333333995,0.,21.424103566632));
#32521=CARTESIAN_POINT('Ctrl Pts',(1.83333333333995,-1.83333333333994,21.424103566632));
#32522=CARTESIAN_POINT('Ctrl Pts',(-2.62369598574772E-15,-1.83333333333994,
21.424103566632));
#32523=CARTESIAN_POINT('Ctrl Pts',(-1.83333333333994,-1.83333333333994,
21.424103566632));
#32524=CARTESIAN_POINT('Ctrl Pts',(-1.83333333333996,0.,21.424103566632));
#32525=CARTESIAN_POINT('Ctrl Pts',(-1.00000000000663,0.,21.3252814375118));
#32526=CARTESIAN_POINT('Ctrl Pts',(-1.0000000000066,1.0000000000066,21.3252814375118));
#32527=CARTESIAN_POINT('Ctrl Pts',(-2.61159376533653E-15,1.0000000000066,
21.3252814375118));
#32528=CARTESIAN_POINT('Ctrl Pts',(1.00000000000662,1.0000000000066,21.3252814375118));
#32529=CARTESIAN_POINT('Ctrl Pts',(1.00000000000662,0.,21.3252814375118));
#32530=CARTESIAN_POINT('Ctrl Pts',(1.00000000000662,-1.0000000000066,21.3252814375118));
#32531=CARTESIAN_POINT('Ctrl Pts',(-2.61159376533653E-15,-1.0000000000066,
21.3252814375118));
#32532=CARTESIAN_POINT('Ctrl Pts',(-1.0000000000066,-1.0000000000066,21.3252814375118));
#32533=CARTESIAN_POINT('Ctrl Pts',(-1.00000000000663,0.,21.3252814375118));
#32534=CARTESIAN_POINT('',(-12.0671767507335,0.,23.306919910827));
#32535=CARTESIAN_POINT('Ctrl Pts',(-2.49999999999985,0.,21.5031612699274));
#32536=CARTESIAN_POINT('Ctrl Pts',(-2.83333333333544,3.69612852901595E-47,
21.5426901215757));
#32537=CARTESIAN_POINT('Ctrl Pts',(-3.16666666667104,-5.17457994063246E-47,
21.5822189732241));
#32538=CARTESIAN_POINT('Ctrl Pts',(-3.50000000000663,0.,21.6217478248724));
#32539=CARTESIAN_POINT('Ctrl Pts',(-4.84782034806848,1.63733269291844E-31,
21.7815811966328));
#32540=CARTESIAN_POINT('Ctrl Pts',(-6.33330197010078,-4.7731456426033E-46,
22.0645075583296));
#32541=CARTESIAN_POINT('Ctrl Pts',(-7.85305095226366,0.,22.4018903191022));
#32542=CARTESIAN_POINT('Ctrl Pts',(-9.31567463360365,3.14633330838416E-31,
22.7265913199738));
#32543=CARTESIAN_POINT('Ctrl Pts',(-10.7340225064793,-6.85272008724022E-46,
23.051417461952));
#32544=CARTESIAN_POINT('Ctrl Pts',(-11.9803472472225,0.,23.2903377571183));
#32545=CARTESIAN_POINT('Ctrl Pts',(-12.0093666549873,4.05611743704363E-31,
23.2959007739165));
#32546=CARTESIAN_POINT('Ctrl Pts',(-12.0383097771307,-1.61138616161747E-47,
23.3014281454301));
#32547=CARTESIAN_POINT('Ctrl Pts',(-12.0671767507335,0.,23.3069199108271));
#32548=CARTESIAN_POINT('',(12.0671767507335,-1.47780293825311E-15,23.306919910827));
#32549=CARTESIAN_POINT('Origin',(-2.85427448667781E-15,0.,23.306919910827));
#32550=CARTESIAN_POINT('Origin',(-2.85427448667781E-15,0.,23.306919910827));
#32551=CARTESIAN_POINT('Origin',(-2.6374721847239E-15,0.,21.5365947680606));
#32552=CARTESIAN_POINT('Origin',(13.4131653526691,-1.64263900155804E-15,
21.5365947680606));
#33464=UNCERTAINTY_MEASURE_WITH_UNIT(LENGTH_MEASURE(0.01),#33475,
'DISTANCE_ACCURACY_VALUE',
'Maximum model space distance between geometric entities at asserted c
onnectivities');
#33467=UNCERTAINTY_MEASURE_WITH_UNIT(LENGTH_MEASURE(0.01),#33475,
'DISTANCE_ACCURACY_VALUE',
'Maximum model space distance between geometric entities at asserted c
onnectivities');
#33471=(
GEOMETRIC_REPRESENTATION_CONTEXT(3)
GLOBAL_UNCERTAINTY_ASSIGNED_CONTEXT((#33464))
GLOBAL_UNIT_ASSIGNED_CONTEXT((#33475,#33477,#33478))
REPRESENTATION_CONTEXT('','3D')
);
#33474=(
GEOMETRIC_REPRESENTATION_CONTEXT(3)
GLOBAL_UNCERTAINTY_ASSIGNED_CONTEXT((#33467))
GLOBAL_UNIT_ASSIGNED_CONTEXT((#33475,#33477,#33478))
REPRESENTATION_CONTEXT('','3D')
);
#33475=(
LENGTH_UNIT()
NAMED_UNIT(*)
SI_UNIT(.MILLI.,.METRE.)
);
#33477=(
NAMED_UNIT(*)
PLANE_ANGLE_UNIT()
SI_UNIT($,.RADIAN.)
);
#33478=(
NAMED_UNIT(*)
SI_UNIT($,.STERADIAN.)
SOLID_ANGLE_UNIT()
);
#33482=SHAPE_DEFINITION_REPRESENTATION(#33488,#33499);
#33488=PRODUCT_DEFINITION_SHAPE('',$,#33506);
#33499=SHAPE_REPRESENTATION('',(#3107),#33471);
#33502=PRODUCT_DEFINITION_CONTEXT('part definition',#33522,'design');
#33506=PRODUCT_DEFINITION('Disc_02','Disc_02',#33512,#33502);
#33512=PRODUCT_DEFINITION_FORMATION('',$,#33527);
#33522=APPLICATION_CONTEXT(
'Core Data for Automotive Mechanical Design Process');
#33523=PRODUCT_CONTEXT('part definition',#33522,'mechanical');
#33527=PRODUCT('Disc_02','Disc_02',$,(#33523));
#33531=PRESENTATION_STYLE_ASSIGNMENT((#33533));
#33533=SURFACE_STYLE_USAGE(.BOTH.,#33535);
#33535=SURFACE_SIDE_STYLE('',(#33537));
#33537=SURFACE_STYLE_FILL_AREA(#33539);
#33539=FILL_AREA_STYLE('Opaque(203,203,203)',(#33541));
#33541=FILL_AREA_STYLE_COLOUR('Opaque(203,203,203)',#33543);
#33543=COLOUR_RGB('Opaque(203,203,203)', 0.09019608, 0.27058824, 0.51372549);
ENDSEC;
END-ISO-10303-21;
